ISO-10303-21;
HEADER;
/* Generated by software containing ST-Developer
 * from STEP Tools, Inc. (www.steptools.com) 
 */

FILE_DESCRIPTION(
/* description */ (''),
/* implementation_level */ '2;1');

FILE_NAME(
/* name */ 'M5x14 Steel 4.6 Plain v1 (1).step',
/* time_stamp */ '2026-10-23T22:29:29+06:00',
/* author */ (''),
/* organization */ (''),
/* preprocessor_version */ 'ST-DEVELOPER v20.2',
/* originating_system */ 'Autodesk Translation Framework v15.15.0.0',
/* authorisation */ '');

FILE_SCHEMA (('AUTOMOTIVE_DESIGN { 1 0 10303 214 3 1 1 }'));
ENDSEC;

DATA;
#10=MECHANICAL_DESIGN_GEOMETRIC_PRESENTATION_REPRESENTATION('',(#73),#7047);
#53=SHAPE_REPRESENTATION_RELATIONSHIP('SRR','None',#7086,#63);
#63=ADVANCED_BREP_SHAPE_REPRESENTATION('',(#86),#7038);
#73=STYLED_ITEM('',(#7212),#86);
#86=MANIFOLD_SOLID_BREP('Body1',#3398);
#96=SPHERICAL_SURFACE('',#3636,12.8319377609308);
#101=CONICAL_SURFACE('',#3631,2.33923048454133,0.261799387799147);
#102=CONICAL_SURFACE('',#3640,5.05813690328693,0.0872664626099692);
#108=FACE_BOUND('',#500,.T.);
#126=TOROIDAL_SURFACE('',#3623,2.37846096908266,0.2);
#144=PLANE('',#3585);
#145=PLANE('',#3587);
#146=PLANE('',#3590);
#147=PLANE('',#3595);
#148=PLANE('',#3597);
#149=PLANE('',#3600);
#150=PLANE('',#3606);
#151=PLANE('',#3611);
#152=PLANE('',#3613);
#153=PLANE('',#3615);
#154=PLANE('',#3618);
#155=PLANE('',#3620);
#156=PLANE('',#3622);
#157=PLANE('',#3627);
#158=PLANE('',#3635);
#291=FACE_OUTER_BOUND('',#481,.T.);
#292=FACE_OUTER_BOUND('',#482,.T.);
#293=FACE_OUTER_BOUND('',#483,.T.);
#294=FACE_OUTER_BOUND('',#484,.T.);
#295=FACE_OUTER_BOUND('',#485,.T.);
#296=FACE_OUTER_BOUND('',#486,.T.);
#297=FACE_OUTER_BOUND('',#487,.T.);
#298=FACE_OUTER_BOUND('',#488,.T.);
#299=FACE_OUTER_BOUND('',#489,.T.);
#300=FACE_OUTER_BOUND('',#490,.T.);
#301=FACE_OUTER_BOUND('',#491,.T.);
#302=FACE_OUTER_BOUND('',#492,.T.);
#303=FACE_OUTER_BOUND('',#493,.T.);
#304=FACE_OUTER_BOUND('',#494,.T.);
#305=FACE_OUTER_BOUND('',#495,.T.);
#306=FACE_OUTER_BOUND('',#496,.T.);
#307=FACE_OUTER_BOUND('',#497,.T.);
#308=FACE_OUTER_BOUND('',#498,.T.);
#309=FACE_OUTER_BOUND('',#499,.T.);
#310=FACE_OUTER_BOUND('',#501,.T.);
#311=FACE_OUTER_BOUND('',#502,.T.);
#312=FACE_OUTER_BOUND('',#503,.T.);
#313=FACE_OUTER_BOUND('',#504,.T.);
#314=FACE_OUTER_BOUND('',#505,.T.);
#315=FACE_OUTER_BOUND('',#506,.T.);
#481=EDGE_LOOP('',(#2347,#2348,#2349,#2350,#2351,#2352));
#482=EDGE_LOOP('',(#2353,#2354,#2355));
#483=EDGE_LOOP('',(#2356,#2357,#2358,#2359,#2360,#2361));
#484=EDGE_LOOP('',(#2362,#2363,#2364));
#485=EDGE_LOOP('',(#2365,#2366,#2367,#2368,#2369,#2370));
#486=EDGE_LOOP('',(#2371,#2372,#2373));
#487=EDGE_LOOP('',(#2374,#2375,#2376,#2377,#2378,#2379));
#488=EDGE_LOOP('',(#2380,#2381,#2382));
#489=EDGE_LOOP('',(#2383,#2384,#2385,#2386,#2387,#2388));
#490=EDGE_LOOP('',(#2389,#2390,#2391));
#491=EDGE_LOOP('',(#2392,#2393,#2394,#2395,#2396,#2397));
#492=EDGE_LOOP('',(#2398,#2399,#2400));
#493=EDGE_LOOP('',(#2401,#2402,#2403));
#494=EDGE_LOOP('',(#2404,#2405,#2406,#2407,#2408,#2409,#2410));
#495=EDGE_LOOP('',(#2411,#2412,#2413));
#496=EDGE_LOOP('',(#2414,#2415,#2416,#2417,#2418,#2419));
#497=EDGE_LOOP('',(#2420,#2421,#2422,#2423,#2424,#2425,#2426,#2427));
#498=EDGE_LOOP('',(#2428,#2429,#2430,#2431));
#499=EDGE_LOOP('',(#2432));
#500=EDGE_LOOP('',(#2433));
#501=EDGE_LOOP('',(#2434,#2435,#2436,#2437));
#502=EDGE_LOOP('',(#2438,#2439,#2440,#2441));
#503=EDGE_LOOP('',(#2442,#2443,#2444,#2445));
#504=EDGE_LOOP('',(#2446));
#505=EDGE_LOOP('',(#2447,#2448,#2449,#2450,#2451,#2452,#2453,#2454,#2455,
#2456,#2457,#2458,#2459,#2460,#2461,#2462,#2463,#2464,#2465,#2466,#2467));
#506=EDGE_LOOP('',(#2468,#2469,#2470,#2471,#2472));
#689=CIRCLE('',#3583,0.946);
#690=CIRCLE('',#3586,12.8232171353527);
#691=CIRCLE('',#3588,12.1073709048319);
#692=CIRCLE('',#3591,12.8232171353527);
#693=CIRCLE('',#3593,0.946);
#694=CIRCLE('',#3596,12.8232171353527);
#695=CIRCLE('',#3598,12.1073709048319);
#696=CIRCLE('',#3601,12.8232171353527);
#697=CIRCLE('',#3604,0.946);
#698=CIRCLE('',#3607,12.8232171353527);
#699=CIRCLE('',#3609,0.946);
#700=CIRCLE('',#3612,12.8232171353527);
#701=CIRCLE('',#3614,12.8232171353527);
#702=CIRCLE('',#3616,12.1073709048319);
#703=CIRCLE('',#3617,12.1073709048319);
#704=CIRCLE('',#3619,12.8232171353527);
#705=CIRCLE('',#3621,12.1073709048319);
#706=CIRCLE('',#3624,2.37846096908266);
#707=CIRCLE('',#3625,0.2);
#708=CIRCLE('',#3626,2.17846096908266);
#709=CIRCLE('',#3628,5.15);
#710=CIRCLE('',#3630,2.17846096908266);
#711=CIRCLE('',#3632,2.4505);
#712=CIRCLE('',#3634,2.4505);
#713=CIRCLE('',#3637,12.8319377609308);
#714=CIRCLE('',#3638,4.96627380657387);
#715=CIRCLE('',#3639,4.96627380657387);
#803=ELLIPSE('',#3582,1.892,0.946);
#804=ELLIPSE('',#3584,1.892,0.946);
#805=ELLIPSE('',#3589,1.892,0.946);
#806=ELLIPSE('',#3594,1.892,0.946);
#807=ELLIPSE('',#3599,1.892,0.946);
#808=ELLIPSE('',#3603,1.892,0.946);
#809=ELLIPSE('',#3605,1.892,0.946);
#810=ELLIPSE('',#3610,1.892,0.946);
#851=LINE('',#5141,#1145);
#852=LINE('',#5148,#1146);
#853=LINE('',#5152,#1147);
#854=LINE('',#5157,#1148);
#855=LINE('',#5160,#1149);
#856=LINE('',#5164,#1150);
#857=LINE('',#5186,#1151);
#858=LINE('',#5190,#1152);
#859=LINE('',#5195,#1153);
#860=LINE('',#5198,#1154);
#861=LINE('',#5202,#1155);
#862=LINE('',#5222,#1156);
#863=LINE('',#5229,#1157);
#864=LINE('',#5233,#1158);
#865=LINE('',#5255,#1159);
#866=LINE('',#5259,#1160);
#867=LINE('',#5263,#1161);
#868=LINE('',#5267,#1162);
#869=LINE('',#5272,#1163);
#870=LINE('',#5275,#1164);
#871=LINE('',#5289,#1165);
#872=LINE('',#5293,#1166);
#873=LINE('',#5297,#1167);
#874=LINE('',#5306,#1168);
#1145=VECTOR('',#4044,10.);
#1146=VECTOR('',#4051,10.);
#1147=VECTOR('',#4056,10.);
#1148=VECTOR('',#4061,10.);
#1149=VECTOR('',#4064,10.);
#1150=VECTOR('',#4069,10.);
#1151=VECTOR('',#4076,10.);
#1152=VECTOR('',#4081,10.);
#1153=VECTOR('',#4086,10.);
#1154=VECTOR('',#4089,10.);
#1155=VECTOR('',#4094,10.);
#1156=VECTOR('',#4097,10.);
#1157=VECTOR('',#4104,10.);
#1158=VECTOR('',#4109,10.);
#1159=VECTOR('',#4116,10.);
#1160=VECTOR('',#4121,10.);
#1161=VECTOR('',#4126,10.);
#1162=VECTOR('',#4131,10.);
#1163=VECTOR('',#4138,10.);
#1164=VECTOR('',#4143,10.);
#1165=VECTOR('',#4162,2.17846096908266);
#1166=VECTOR('',#4167,2.33923048454133);
#1167=VECTOR('',#4172,2.5);
#1168=VECTOR('',#4185,5.05813690328693);
#1419=B_SPLINE_CURVE_WITH_KNOTS('',3,(#5125,#5126,#5127,#5128,#5129,#5130,
#5131,#5132,#5133,#5134,#5135,#5136,#5137,#5138,#5139),.UNSPECIFIED.,.F.,
 .F.,(4,2,2,3,2,2,4),(-0.0714521071173775,-0.0712222400952786,-0.0356111200476392,
0.,0.0356111200476392,0.0712222400952784,0.0714521071173274),
 .UNSPECIFIED.);
#1420=B_SPLINE_CURVE_WITH_KNOTS('',3,(#5167,#5168,#5169,#5170,#5171,#5172,
#5173,#5174,#5175,#5176,#5177,#5178,#5179,#5180,#5181),.UNSPECIFIED.,.F.,
 .F.,(4,2,2,3,2,2,4),(-0.071452107117379,-0.0712222400952786,-0.0356111200476392,
0.,0.0356111200476392,0.0712222400952784,0.071452107117329),
 .UNSPECIFIED.);
#1421=B_SPLINE_CURVE_WITH_KNOTS('',3,(#5206,#5207,#5208,#5209,#5210,#5211,
#5212,#5213,#5214,#5215,#5216,#5217,#5218,#5219,#5220),.UNSPECIFIED.,.F.,
 .F.,(4,2,2,3,2,2,4),(-0.0714521071173781,-0.0712222400952784,-0.0356111200476392,
0.,0.0356111200476392,0.0712222400952785,0.0714521071173282),
 .UNSPECIFIED.);
#1422=B_SPLINE_CURVE_WITH_KNOTS('',3,(#5236,#5237,#5238,#5239,#5240,#5241,
#5242,#5243,#5244,#5245,#5246,#5247,#5248,#5249,#5250),.UNSPECIFIED.,.F.,
 .F.,(4,2,2,3,2,2,4),(-0.0714521071173768,-0.0712222400952786,-0.0356111200476392,
0.,0.0356111200476392,0.0712222400952785,0.0714521071173268),
 .UNSPECIFIED.);
#1473=VERTEX_POINT('',#5123);
#1474=VERTEX_POINT('',#5124);
#1475=VERTEX_POINT('',#5140);
#1476=VERTEX_POINT('',#5142);
#1477=VERTEX_POINT('',#5144);
#1478=VERTEX_POINT('',#5146);
#1479=VERTEX_POINT('',#5150);
#1480=VERTEX_POINT('',#5154);
#1481=VERTEX_POINT('',#5156);
#1482=VERTEX_POINT('',#5158);
#1483=VERTEX_POINT('',#5162);
#1484=VERTEX_POINT('',#5166);
#1485=VERTEX_POINT('',#5182);
#1486=VERTEX_POINT('',#5184);
#1487=VERTEX_POINT('',#5188);
#1488=VERTEX_POINT('',#5192);
#1489=VERTEX_POINT('',#5194);
#1490=VERTEX_POINT('',#5196);
#1491=VERTEX_POINT('',#5200);
#1492=VERTEX_POINT('',#5204);
#1493=VERTEX_POINT('',#5205);
#1494=VERTEX_POINT('',#5221);
#1495=VERTEX_POINT('',#5223);
#1496=VERTEX_POINT('',#5225);
#1497=VERTEX_POINT('',#5227);
#1498=VERTEX_POINT('',#5231);
#1499=VERTEX_POINT('',#5235);
#1500=VERTEX_POINT('',#5251);
#1501=VERTEX_POINT('',#5253);
#1502=VERTEX_POINT('',#5257);
#1503=VERTEX_POINT('',#5261);
#1504=VERTEX_POINT('',#5265);
#1505=VERTEX_POINT('',#5270);
#1506=VERTEX_POINT('',#5278);
#1507=VERTEX_POINT('',#5280);
#1508=VERTEX_POINT('',#5284);
#1509=VERTEX_POINT('',#5287);
#1510=VERTEX_POINT('',#5291);
#1511=VERTEX_POINT('',#5295);
#1512=VERTEX_POINT('',#5300);
#1513=VERTEX_POINT('',#5302);
#1808=EDGE_CURVE('',#1473,#1474,#1419,.T.);
#1809=EDGE_CURVE('',#1475,#1473,#851,.T.);
#1810=EDGE_CURVE('',#1475,#1476,#803,.F.);
#1811=EDGE_CURVE('',#1476,#1477,#689,.F.);
#1812=EDGE_CURVE('',#1478,#1477,#804,.T.);
#1813=EDGE_CURVE('',#1474,#1478,#852,.T.);
#1814=EDGE_CURVE('',#1474,#1479,#690,.T.);
#1815=EDGE_CURVE('',#1479,#1478,#853,.F.);
#1816=EDGE_CURVE('',#1479,#1480,#691,.T.);
#1817=EDGE_CURVE('',#1477,#1481,#854,.F.);
#1818=EDGE_CURVE('',#1482,#1481,#805,.F.);
#1819=EDGE_CURVE('',#1480,#1482,#855,.T.);
#1820=EDGE_CURVE('',#1480,#1483,#692,.T.);
#1821=EDGE_CURVE('',#1482,#1483,#856,.T.);
#1822=EDGE_CURVE('',#1483,#1484,#1420,.T.);
#1823=EDGE_CURVE('',#1481,#1485,#693,.F.);
#1824=EDGE_CURVE('',#1486,#1485,#806,.T.);
#1825=EDGE_CURVE('',#1484,#1486,#857,.T.);
#1826=EDGE_CURVE('',#1484,#1487,#694,.T.);
#1827=EDGE_CURVE('',#1487,#1486,#858,.F.);
#1828=EDGE_CURVE('',#1487,#1488,#695,.T.);
#1829=EDGE_CURVE('',#1485,#1489,#859,.F.);
#1830=EDGE_CURVE('',#1490,#1489,#807,.F.);
#1831=EDGE_CURVE('',#1488,#1490,#860,.T.);
#1832=EDGE_CURVE('',#1488,#1491,#696,.T.);
#1833=EDGE_CURVE('',#1490,#1491,#861,.T.);
#1834=EDGE_CURVE('',#1492,#1493,#1421,.T.);
#1835=EDGE_CURVE('',#1494,#1492,#862,.T.);
#1836=EDGE_CURVE('',#1494,#1495,#808,.F.);
#1837=EDGE_CURVE('',#1495,#1496,#697,.F.);
#1838=EDGE_CURVE('',#1497,#1496,#809,.T.);
#1839=EDGE_CURVE('',#1493,#1497,#863,.T.);
#1840=EDGE_CURVE('',#1493,#1498,#698,.T.);
#1841=EDGE_CURVE('',#1498,#1497,#864,.F.);
#1842=EDGE_CURVE('',#1491,#1499,#1422,.T.);
#1843=EDGE_CURVE('',#1489,#1500,#699,.F.);
#1844=EDGE_CURVE('',#1501,#1500,#810,.T.);
#1845=EDGE_CURVE('',#1499,#1501,#865,.T.);
#1846=EDGE_CURVE('',#1499,#1502,#700,.T.);
#1847=EDGE_CURVE('',#1502,#1501,#866,.F.);
#1848=EDGE_CURVE('',#1503,#1473,#701,.T.);
#1849=EDGE_CURVE('',#1503,#1475,#867,.T.);
#1850=EDGE_CURVE('',#1498,#1504,#702,.T.);
#1851=EDGE_CURVE('',#1496,#1476,#868,.F.);
#1852=EDGE_CURVE('',#1504,#1503,#703,.T.);
#1853=EDGE_CURVE('',#1505,#1492,#704,.T.);
#1854=EDGE_CURVE('',#1505,#1494,#869,.T.);
#1855=EDGE_CURVE('',#1502,#1505,#705,.T.);
#1856=EDGE_CURVE('',#1500,#1495,#870,.F.);
#1857=EDGE_CURVE('',#1506,#1506,#706,.T.);
#1858=EDGE_CURVE('',#1506,#1507,#707,.T.);
#1859=EDGE_CURVE('',#1507,#1507,#708,.T.);
#1860=EDGE_CURVE('',#1508,#1508,#709,.T.);
#1861=EDGE_CURVE('',#1509,#1509,#710,.T.);
#1862=EDGE_CURVE('',#1509,#1507,#871,.T.);
#1863=EDGE_CURVE('',#1510,#1510,#711,.T.);
#1864=EDGE_CURVE('',#1510,#1509,#872,.T.);
#1865=EDGE_CURVE('',#1511,#1511,#712,.F.);
#1866=EDGE_CURVE('',#1511,#1510,#873,.T.);
#1867=EDGE_CURVE('',#1504,#1512,#713,.T.);
#1868=EDGE_CURVE('',#1513,#1512,#714,.T.);
#1869=EDGE_CURVE('',#1512,#1513,#715,.T.);
#1870=EDGE_CURVE('',#1508,#1513,#874,.T.);
#2347=ORIENTED_EDGE('',*,*,#1808,.F.);
#2348=ORIENTED_EDGE('',*,*,#1809,.F.);
#2349=ORIENTED_EDGE('',*,*,#1810,.T.);
#2350=ORIENTED_EDGE('',*,*,#1811,.T.);
#2351=ORIENTED_EDGE('',*,*,#1812,.F.);
#2352=ORIENTED_EDGE('',*,*,#1813,.F.);
#2353=ORIENTED_EDGE('',*,*,#1814,.F.);
#2354=ORIENTED_EDGE('',*,*,#1813,.T.);
#2355=ORIENTED_EDGE('',*,*,#1815,.F.);
#2356=ORIENTED_EDGE('',*,*,#1816,.F.);
#2357=ORIENTED_EDGE('',*,*,#1815,.T.);
#2358=ORIENTED_EDGE('',*,*,#1812,.T.);
#2359=ORIENTED_EDGE('',*,*,#1817,.T.);
#2360=ORIENTED_EDGE('',*,*,#1818,.F.);
#2361=ORIENTED_EDGE('',*,*,#1819,.F.);
#2362=ORIENTED_EDGE('',*,*,#1820,.F.);
#2363=ORIENTED_EDGE('',*,*,#1819,.T.);
#2364=ORIENTED_EDGE('',*,*,#1821,.T.);
#2365=ORIENTED_EDGE('',*,*,#1822,.F.);
#2366=ORIENTED_EDGE('',*,*,#1821,.F.);
#2367=ORIENTED_EDGE('',*,*,#1818,.T.);
#2368=ORIENTED_EDGE('',*,*,#1823,.T.);
#2369=ORIENTED_EDGE('',*,*,#1824,.F.);
#2370=ORIENTED_EDGE('',*,*,#1825,.F.);
#2371=ORIENTED_EDGE('',*,*,#1826,.F.);
#2372=ORIENTED_EDGE('',*,*,#1825,.T.);
#2373=ORIENTED_EDGE('',*,*,#1827,.F.);
#2374=ORIENTED_EDGE('',*,*,#1828,.F.);
#2375=ORIENTED_EDGE('',*,*,#1827,.T.);
#2376=ORIENTED_EDGE('',*,*,#1824,.T.);
#2377=ORIENTED_EDGE('',*,*,#1829,.T.);
#2378=ORIENTED_EDGE('',*,*,#1830,.F.);
#2379=ORIENTED_EDGE('',*,*,#1831,.F.);
#2380=ORIENTED_EDGE('',*,*,#1832,.F.);
#2381=ORIENTED_EDGE('',*,*,#1831,.T.);
#2382=ORIENTED_EDGE('',*,*,#1833,.T.);
#2383=ORIENTED_EDGE('',*,*,#1834,.F.);
#2384=ORIENTED_EDGE('',*,*,#1835,.F.);
#2385=ORIENTED_EDGE('',*,*,#1836,.T.);
#2386=ORIENTED_EDGE('',*,*,#1837,.T.);
#2387=ORIENTED_EDGE('',*,*,#1838,.F.);
#2388=ORIENTED_EDGE('',*,*,#1839,.F.);
#2389=ORIENTED_EDGE('',*,*,#1840,.F.);
#2390=ORIENTED_EDGE('',*,*,#1839,.T.);
#2391=ORIENTED_EDGE('',*,*,#1841,.F.);
#2392=ORIENTED_EDGE('',*,*,#1842,.F.);
#2393=ORIENTED_EDGE('',*,*,#1833,.F.);
#2394=ORIENTED_EDGE('',*,*,#1830,.T.);
#2395=ORIENTED_EDGE('',*,*,#1843,.T.);
#2396=ORIENTED_EDGE('',*,*,#1844,.F.);
#2397=ORIENTED_EDGE('',*,*,#1845,.F.);
#2398=ORIENTED_EDGE('',*,*,#1846,.F.);
#2399=ORIENTED_EDGE('',*,*,#1845,.T.);
#2400=ORIENTED_EDGE('',*,*,#1847,.F.);
#2401=ORIENTED_EDGE('',*,*,#1848,.F.);
#2402=ORIENTED_EDGE('',*,*,#1849,.T.);
#2403=ORIENTED_EDGE('',*,*,#1809,.T.);
#2404=ORIENTED_EDGE('',*,*,#1850,.F.);
#2405=ORIENTED_EDGE('',*,*,#1841,.T.);
#2406=ORIENTED_EDGE('',*,*,#1838,.T.);
#2407=ORIENTED_EDGE('',*,*,#1851,.T.);
#2408=ORIENTED_EDGE('',*,*,#1810,.F.);
#2409=ORIENTED_EDGE('',*,*,#1849,.F.);
#2410=ORIENTED_EDGE('',*,*,#1852,.F.);
#2411=ORIENTED_EDGE('',*,*,#1853,.F.);
#2412=ORIENTED_EDGE('',*,*,#1854,.T.);
#2413=ORIENTED_EDGE('',*,*,#1835,.T.);
#2414=ORIENTED_EDGE('',*,*,#1855,.F.);
#2415=ORIENTED_EDGE('',*,*,#1847,.T.);
#2416=ORIENTED_EDGE('',*,*,#1844,.T.);
#2417=ORIENTED_EDGE('',*,*,#1856,.T.);
#2418=ORIENTED_EDGE('',*,*,#1836,.F.);
#2419=ORIENTED_EDGE('',*,*,#1854,.F.);
#2420=ORIENTED_EDGE('',*,*,#1817,.F.);
#2421=ORIENTED_EDGE('',*,*,#1811,.F.);
#2422=ORIENTED_EDGE('',*,*,#1851,.F.);
#2423=ORIENTED_EDGE('',*,*,#1837,.F.);
#2424=ORIENTED_EDGE('',*,*,#1856,.F.);
#2425=ORIENTED_EDGE('',*,*,#1843,.F.);
#2426=ORIENTED_EDGE('',*,*,#1829,.F.);
#2427=ORIENTED_EDGE('',*,*,#1823,.F.);
#2428=ORIENTED_EDGE('',*,*,#1857,.T.);
#2429=ORIENTED_EDGE('',*,*,#1858,.T.);
#2430=ORIENTED_EDGE('',*,*,#1859,.T.);
#2431=ORIENTED_EDGE('',*,*,#1858,.F.);
#2432=ORIENTED_EDGE('',*,*,#1860,.T.);
#2433=ORIENTED_EDGE('',*,*,#1857,.F.);
#2434=ORIENTED_EDGE('',*,*,#1861,.F.);
#2435=ORIENTED_EDGE('',*,*,#1862,.T.);
#2436=ORIENTED_EDGE('',*,*,#1859,.F.);
#2437=ORIENTED_EDGE('',*,*,#1862,.F.);
#2438=ORIENTED_EDGE('',*,*,#1863,.F.);
#2439=ORIENTED_EDGE('',*,*,#1864,.T.);
#2440=ORIENTED_EDGE('',*,*,#1861,.T.);
#2441=ORIENTED_EDGE('',*,*,#1864,.F.);
#2442=ORIENTED_EDGE('',*,*,#1865,.F.);
#2443=ORIENTED_EDGE('',*,*,#1866,.T.);
#2444=ORIENTED_EDGE('',*,*,#1863,.T.);
#2445=ORIENTED_EDGE('',*,*,#1866,.F.);
#2446=ORIENTED_EDGE('',*,*,#1865,.T.);
#2447=ORIENTED_EDGE('',*,*,#1842,.T.);
#2448=ORIENTED_EDGE('',*,*,#1846,.T.);
#2449=ORIENTED_EDGE('',*,*,#1855,.T.);
#2450=ORIENTED_EDGE('',*,*,#1853,.T.);
#2451=ORIENTED_EDGE('',*,*,#1834,.T.);
#2452=ORIENTED_EDGE('',*,*,#1840,.T.);
#2453=ORIENTED_EDGE('',*,*,#1850,.T.);
#2454=ORIENTED_EDGE('',*,*,#1867,.T.);
#2455=ORIENTED_EDGE('',*,*,#1868,.F.);
#2456=ORIENTED_EDGE('',*,*,#1869,.F.);
#2457=ORIENTED_EDGE('',*,*,#1867,.F.);
#2458=ORIENTED_EDGE('',*,*,#1852,.T.);
#2459=ORIENTED_EDGE('',*,*,#1848,.T.);
#2460=ORIENTED_EDGE('',*,*,#1808,.T.);
#2461=ORIENTED_EDGE('',*,*,#1814,.T.);
#2462=ORIENTED_EDGE('',*,*,#1816,.T.);
#2463=ORIENTED_EDGE('',*,*,#1820,.T.);
#2464=ORIENTED_EDGE('',*,*,#1822,.T.);
#2465=ORIENTED_EDGE('',*,*,#1826,.T.);
#2466=ORIENTED_EDGE('',*,*,#1828,.T.);
#2467=ORIENTED_EDGE('',*,*,#1832,.T.);
#2468=ORIENTED_EDGE('',*,*,#1860,.F.);
#2469=ORIENTED_EDGE('',*,*,#1870,.T.);
#2470=ORIENTED_EDGE('',*,*,#1868,.T.);
#2471=ORIENTED_EDGE('',*,*,#1869,.T.);
#2472=ORIENTED_EDGE('',*,*,#1870,.F.);
#3179=CYLINDRICAL_SURFACE('',#3581,0.946);
#3180=CYLINDRICAL_SURFACE('',#3592,0.946);
#3181=CYLINDRICAL_SURFACE('',#3602,0.946);
#3182=CYLINDRICAL_SURFACE('',#3608,0.946);
#3183=CYLINDRICAL_SURFACE('',#3629,2.17846096908266);
#3184=CYLINDRICAL_SURFACE('',#3633,2.4505);
#3233=ADVANCED_FACE('',(#291),#3179,.T.);
#3234=ADVANCED_FACE('',(#292),#144,.F.);
#3235=ADVANCED_FACE('',(#293),#145,.F.);
#3236=ADVANCED_FACE('',(#294),#146,.F.);
#3237=ADVANCED_FACE('',(#295),#3180,.T.);
#3238=ADVANCED_FACE('',(#296),#147,.F.);
#3239=ADVANCED_FACE('',(#297),#148,.F.);
#3240=ADVANCED_FACE('',(#298),#149,.F.);
#3241=ADVANCED_FACE('',(#299),#3181,.T.);
#3242=ADVANCED_FACE('',(#300),#150,.F.);
#3243=ADVANCED_FACE('',(#301),#3182,.T.);
#3244=ADVANCED_FACE('',(#302),#151,.F.);
#3245=ADVANCED_FACE('',(#303),#152,.F.);
#3246=ADVANCED_FACE('',(#304),#153,.F.);
#3247=ADVANCED_FACE('',(#305),#154,.F.);
#3248=ADVANCED_FACE('',(#306),#155,.F.);
#3249=ADVANCED_FACE('',(#307),#156,.F.);
#3250=ADVANCED_FACE('',(#308),#126,.F.);
#3251=ADVANCED_FACE('',(#309,#108),#157,.T.);
#3252=ADVANCED_FACE('',(#310),#3183,.T.);
#3253=ADVANCED_FACE('',(#311),#101,.T.);
#3254=ADVANCED_FACE('',(#312),#3184,.T.);
#3255=ADVANCED_FACE('',(#313),#158,.T.);
#3256=ADVANCED_FACE('',(#314),#96,.T.);
#3257=ADVANCED_FACE('',(#315),#102,.T.);
#3398=CLOSED_SHELL('',(#3233,#3234,#3235,#3236,#3237,#3238,#3239,#3240,
#3241,#3242,#3243,#3244,#3245,#3246,#3247,#3248,#3249,#3250,#3251,#3252,
#3253,#3254,#3255,#3256,#3257));
#3580=AXIS2_PLACEMENT_3D('',#5121,#4040,#4041);
#3581=AXIS2_PLACEMENT_3D('',#5122,#4042,#4043);
#3582=AXIS2_PLACEMENT_3D('',#5143,#4045,#4046);
#3583=AXIS2_PLACEMENT_3D('',#5145,#4047,#4048);
#3584=AXIS2_PLACEMENT_3D('',#5147,#4049,#4050);
#3585=AXIS2_PLACEMENT_3D('',#5149,#4052,#4053);
#3586=AXIS2_PLACEMENT_3D('',#5151,#4054,#4055);
#3587=AXIS2_PLACEMENT_3D('',#5153,#4057,#4058);
#3588=AXIS2_PLACEMENT_3D('',#5155,#4059,#4060);
#3589=AXIS2_PLACEMENT_3D('',#5159,#4062,#4063);
#3590=AXIS2_PLACEMENT_3D('',#5161,#4065,#4066);
#3591=AXIS2_PLACEMENT_3D('',#5163,#4067,#4068);
#3592=AXIS2_PLACEMENT_3D('',#5165,#4070,#4071);
#3593=AXIS2_PLACEMENT_3D('',#5183,#4072,#4073);
#3594=AXIS2_PLACEMENT_3D('',#5185,#4074,#4075);
#3595=AXIS2_PLACEMENT_3D('',#5187,#4077,#4078);
#3596=AXIS2_PLACEMENT_3D('',#5189,#4079,#4080);
#3597=AXIS2_PLACEMENT_3D('',#5191,#4082,#4083);
#3598=AXIS2_PLACEMENT_3D('',#5193,#4084,#4085);
#3599=AXIS2_PLACEMENT_3D('',#5197,#4087,#4088);
#3600=AXIS2_PLACEMENT_3D('',#5199,#4090,#4091);
#3601=AXIS2_PLACEMENT_3D('',#5201,#4092,#4093);
#3602=AXIS2_PLACEMENT_3D('',#5203,#4095,#4096);
#3603=AXIS2_PLACEMENT_3D('',#5224,#4098,#4099);
#3604=AXIS2_PLACEMENT_3D('',#5226,#4100,#4101);
#3605=AXIS2_PLACEMENT_3D('',#5228,#4102,#4103);
#3606=AXIS2_PLACEMENT_3D('',#5230,#4105,#4106);
#3607=AXIS2_PLACEMENT_3D('',#5232,#4107,#4108);
#3608=AXIS2_PLACEMENT_3D('',#5234,#4110,#4111);
#3609=AXIS2_PLACEMENT_3D('',#5252,#4112,#4113);
#3610=AXIS2_PLACEMENT_3D('',#5254,#4114,#4115);
#3611=AXIS2_PLACEMENT_3D('',#5256,#4117,#4118);
#3612=AXIS2_PLACEMENT_3D('',#5258,#4119,#4120);
#3613=AXIS2_PLACEMENT_3D('',#5260,#4122,#4123);
#3614=AXIS2_PLACEMENT_3D('',#5262,#4124,#4125);
#3615=AXIS2_PLACEMENT_3D('',#5264,#4127,#4128);
#3616=AXIS2_PLACEMENT_3D('',#5266,#4129,#4130);
#3617=AXIS2_PLACEMENT_3D('',#5268,#4132,#4133);
#3618=AXIS2_PLACEMENT_3D('',#5269,#4134,#4135);
#3619=AXIS2_PLACEMENT_3D('',#5271,#4136,#4137);
#3620=AXIS2_PLACEMENT_3D('',#5273,#4139,#4140);
#3621=AXIS2_PLACEMENT_3D('',#5274,#4141,#4142);
#3622=AXIS2_PLACEMENT_3D('',#5276,#4144,#4145);
#3623=AXIS2_PLACEMENT_3D('',#5277,#4146,#4147);
#3624=AXIS2_PLACEMENT_3D('',#5279,#4148,#4149);
#3625=AXIS2_PLACEMENT_3D('',#5281,#4150,#4151);
#3626=AXIS2_PLACEMENT_3D('',#5282,#4152,#4153);
#3627=AXIS2_PLACEMENT_3D('',#5283,#4154,#4155);
#3628=AXIS2_PLACEMENT_3D('',#5285,#4156,#4157);
#3629=AXIS2_PLACEMENT_3D('',#5286,#4158,#4159);
#3630=AXIS2_PLACEMENT_3D('',#5288,#4160,#4161);
#3631=AXIS2_PLACEMENT_3D('',#5290,#4163,#4164);
#3632=AXIS2_PLACEMENT_3D('',#5292,#4165,#4166);
#3633=AXIS2_PLACEMENT_3D('',#5294,#4168,#4169);
#3634=AXIS2_PLACEMENT_3D('',#5296,#4170,#4171);
#3635=AXIS2_PLACEMENT_3D('',#5298,#4173,#4174);
#3636=AXIS2_PLACEMENT_3D('',#5299,#4175,#4176);
#3637=AXIS2_PLACEMENT_3D('',#5301,#4177,#4178);
#3638=AXIS2_PLACEMENT_3D('',#5303,#4179,#4180);
#3639=AXIS2_PLACEMENT_3D('',#5304,#4181,#4182);
#3640=AXIS2_PLACEMENT_3D('',#5305,#4183,#4184);
#4040=DIRECTION('axis',(0.,0.,1.));
#4041=DIRECTION('refdir',(1.,0.,0.));
#4042=DIRECTION('center_axis',(0.,0.,-1.));
#4043=DIRECTION('ref_axis',(0.707106781186563,-0.707106781186532,0.));
#4044=DIRECTION('',(0.,0.,1.));
#4045=DIRECTION('center_axis',(-0.866025403784439,0.,-0.5));
#4046=DIRECTION('ref_axis',(0.5,0.,-0.866025403784439));
#4047=DIRECTION('center_axis',(0.,0.,-1.));
#4048=DIRECTION('ref_axis',(0.707106781186563,-0.707106781186532,0.));
#4049=DIRECTION('center_axis',(-2.54091264057109E-15,0.866025403784439,
-0.5));
#4050=DIRECTION('ref_axis',(1.43032168209504E-15,-0.5,-0.866025403784439));
#4051=DIRECTION('',(0.,0.,-1.));
#4052=DIRECTION('center_axis',(-1.,-4.30300426108057E-14,0.));
#4053=DIRECTION('ref_axis',(-4.30300426108057E-14,1.,0.));
#4054=DIRECTION('center_axis',(-1.,-4.30300426108057E-14,0.));
#4055=DIRECTION('ref_axis',(0.,0.,-1.));
#4056=DIRECTION('',(-2.15150213054029E-14,0.5,0.866025403784439));
#4057=DIRECTION('center_axis',(-2.54091264057109E-15,0.866025403784439,
-0.5));
#4058=DIRECTION('ref_axis',(1.,2.93399319404209E-15,0.));
#4059=DIRECTION('center_axis',(-2.54091264057109E-15,0.866025403784439,
-0.5));
#4060=DIRECTION('ref_axis',(0.,-0.5,-0.866025403784439));
#4061=DIRECTION('',(-1.,-2.93399319404209E-15,0.));
#4062=DIRECTION('center_axis',(-2.54091264057109E-15,0.866025403784439,
-0.5));
#4063=DIRECTION('ref_axis',(1.46699659702056E-15,-0.5,-0.866025403784439));
#4064=DIRECTION('',(-1.73044443434865E-14,-0.5,-0.866025403784439));
#4065=DIRECTION('center_axis',(1.,-3.4608888686973E-14,0.));
#4066=DIRECTION('ref_axis',(-3.4608888686973E-14,-1.,0.));
#4067=DIRECTION('center_axis',(1.,-3.4608888686973E-14,0.));
#4068=DIRECTION('ref_axis',(0.,0.,1.));
#4069=DIRECTION('',(0.,0.,1.));
#4070=DIRECTION('center_axis',(0.,0.,-1.));
#4071=DIRECTION('ref_axis',(-0.707106781186546,-0.707106781186549,0.));
#4072=DIRECTION('center_axis',(0.,0.,-1.));
#4073=DIRECTION('ref_axis',(-0.707106781186546,-0.707106781186549,0.));
#4074=DIRECTION('center_axis',(0.866025403784439,0.,-0.5));
#4075=DIRECTION('ref_axis',(-0.5,-3.66749149255139E-17,-0.866025403784439));
#4076=DIRECTION('',(0.,0.,-1.));
#4077=DIRECTION('center_axis',(-4.04626176340286E-14,1.,0.));
#4078=DIRECTION('ref_axis',(1.,4.04626176340286E-14,0.));
#4079=DIRECTION('center_axis',(-4.04626176340286E-14,1.,0.));
#4080=DIRECTION('ref_axis',(0.,0.,-1.));
#4081=DIRECTION('',(0.5,2.02313088170143E-14,0.866025403784439));
#4082=DIRECTION('center_axis',(0.866025403784439,0.,-0.5));
#4083=DIRECTION('ref_axis',(0.,-1.,0.));
#4084=DIRECTION('center_axis',(0.866025403784439,0.,-0.5));
#4085=DIRECTION('ref_axis',(0.5,0.,0.866025403784439));
#4086=DIRECTION('',(0.,1.,0.));
#4087=DIRECTION('center_axis',(0.866025403784439,0.,-0.5));
#4088=DIRECTION('ref_axis',(-0.5,3.66749149255139E-17,-0.866025403784439));
#4089=DIRECTION('',(-0.5,2.39626331165986E-16,-0.866025403784439));
#4090=DIRECTION('center_axis',(-4.79252662331972E-16,-1.,0.));
#4091=DIRECTION('ref_axis',(-1.,4.79252662331972E-16,0.));
#4092=DIRECTION('center_axis',(-4.79252662331972E-16,-1.,0.));
#4093=DIRECTION('ref_axis',(0.,0.,1.));
#4094=DIRECTION('',(0.,0.,1.));
#4095=DIRECTION('center_axis',(0.,0.,-1.));
#4096=DIRECTION('ref_axis',(0.70710678118653,0.707106781186565,0.));
#4097=DIRECTION('',(0.,0.,1.));
#4098=DIRECTION('center_axis',(-1.27045632028555E-15,-0.866025403784439,
-0.5));
#4099=DIRECTION('ref_axis',(6.96823383584764E-16,0.5,-0.866025403784439));
#4100=DIRECTION('center_axis',(0.,0.,-1.));
#4101=DIRECTION('ref_axis',(0.70710678118653,0.707106781186565,0.));
#4102=DIRECTION('center_axis',(-0.866025403784439,0.,-0.5));
#4103=DIRECTION('ref_axis',(0.5,3.66749149255139E-17,-0.866025403784439));
#4104=DIRECTION('',(0.,0.,-1.));
#4105=DIRECTION('center_axis',(5.35736011821097E-14,-1.,0.));
#4106=DIRECTION('ref_axis',(-1.,-5.35736011821097E-14,0.));
#4107=DIRECTION('center_axis',(5.35736011821097E-14,-1.,0.));
#4108=DIRECTION('ref_axis',(0.,0.,1.));
#4109=DIRECTION('',(-0.5,-2.67868005910549E-14,0.866025403784439));
#4110=DIRECTION('center_axis',(0.,0.,-1.));
#4111=DIRECTION('ref_axis',(-0.707106781186557,0.707106781186538,0.));
#4112=DIRECTION('center_axis',(0.,0.,-1.));
#4113=DIRECTION('ref_axis',(-0.707106781186557,0.707106781186538,0.));
#4114=DIRECTION('center_axis',(-1.27045632028555E-15,-0.866025403784439,
-0.5));
#4115=DIRECTION('ref_axis',(7.33498298510278E-16,0.5,-0.866025403784439));
#4116=DIRECTION('',(0.,0.,-1.));
#4117=DIRECTION('center_axis',(1.,2.81047454124667E-14,0.));
#4118=DIRECTION('ref_axis',(2.81047454124667E-14,-1.,0.));
#4119=DIRECTION('center_axis',(1.,2.81047454124667E-14,0.));
#4120=DIRECTION('ref_axis',(0.,0.,1.));
#4121=DIRECTION('',(1.40523727062334E-14,-0.5,0.866025403784439));
#4122=DIRECTION('center_axis',(0.,1.,0.));
#4123=DIRECTION('ref_axis',(1.,0.,0.));
#4124=DIRECTION('center_axis',(0.,1.,0.));
#4125=DIRECTION('ref_axis',(0.,0.,-1.));
#4126=DIRECTION('',(0.5,0.,-0.866025403784439));
#4127=DIRECTION('center_axis',(-0.866025403784439,0.,-0.5));
#4128=DIRECTION('ref_axis',(0.,1.,0.));
#4129=DIRECTION('center_axis',(-0.866025403784439,0.,-0.5));
#4130=DIRECTION('ref_axis',(0.5,0.,-0.866025403784439));
#4131=DIRECTION('',(0.,-1.,0.));
#4132=DIRECTION('center_axis',(-0.866025403784439,0.,-0.5));
#4133=DIRECTION('ref_axis',(0.5,0.,-0.866025403784439));
#4134=DIRECTION('center_axis',(-1.,3.8682536316795E-15,0.));
#4135=DIRECTION('ref_axis',(3.8682536316795E-15,1.,0.));
#4136=DIRECTION('center_axis',(-1.,3.8682536316795E-15,0.));
#4137=DIRECTION('ref_axis',(0.,0.,-1.));
#4138=DIRECTION('',(1.93412681583975E-15,0.5,-0.866025403784439));
#4139=DIRECTION('center_axis',(-1.27045632028555E-15,-0.866025403784439,
-0.5));
#4140=DIRECTION('ref_axis',(-1.,1.46699659702105E-15,0.));
#4141=DIRECTION('center_axis',(-1.27045632028555E-15,-0.866025403784439,
-0.5));
#4142=DIRECTION('ref_axis',(0.,-0.5,0.866025403784439));
#4143=DIRECTION('',(1.,-1.46699659702105E-15,0.));
#4144=DIRECTION('center_axis',(0.,0.,-1.));
#4145=DIRECTION('ref_axis',(-1.,0.,0.));
#4146=DIRECTION('center_axis',(0.,0.,-1.));
#4147=DIRECTION('ref_axis',(-1.,0.,0.));
#4148=DIRECTION('center_axis',(0.,0.,-1.));
#4149=DIRECTION('ref_axis',(1.,0.,0.));
#4150=DIRECTION('center_axis',(-1.22464679914735E-16,-1.,0.));
#4151=DIRECTION('ref_axis',(1.,-1.22464679914735E-16,0.));
#4152=DIRECTION('center_axis',(0.,0.,1.));
#4153=DIRECTION('ref_axis',(1.,0.,0.));
#4154=DIRECTION('center_axis',(0.,0.,-1.));
#4155=DIRECTION('ref_axis',(-1.,0.,0.));
#4156=DIRECTION('center_axis',(0.,0.,-1.));
#4157=DIRECTION('ref_axis',(1.,0.,0.));
#4158=DIRECTION('center_axis',(0.,0.,-1.));
#4159=DIRECTION('ref_axis',(-1.,0.,0.));
#4160=DIRECTION('center_axis',(0.,0.,-1.));
#4161=DIRECTION('ref_axis',(1.,0.,0.));
#4162=DIRECTION('',(0.,0.,1.));
#4163=DIRECTION('center_axis',(0.,0.,-1.));
#4164=DIRECTION('ref_axis',(-1.,0.,0.));
#4165=DIRECTION('center_axis',(0.,0.,-1.));
#4166=DIRECTION('ref_axis',(-1.,0.,0.));
#4167=DIRECTION('',(-0.258819045102519,3.16961915143174E-17,0.965925826289069));
#4168=DIRECTION('center_axis',(0.,0.,-1.));
#4169=DIRECTION('ref_axis',(-1.,0.,0.));
#4170=DIRECTION('center_axis',(0.,0.,1.));
#4171=DIRECTION('ref_axis',(-1.,0.,0.));
#4172=DIRECTION('',(0.,0.,1.));
#4173=DIRECTION('center_axis',(0.,0.,-1.));
#4174=DIRECTION('ref_axis',(-1.,0.,0.));
#4175=DIRECTION('center_axis',(6.12323399573676E-17,0.,1.));
#4176=DIRECTION('ref_axis',(1.,0.,0.));
#4177=DIRECTION('center_axis',(1.22464679914735E-16,-1.,0.));
#4178=DIRECTION('ref_axis',(-1.,-1.22464679914735E-16,0.));
#4179=DIRECTION('center_axis',(0.,0.,-1.));
#4180=DIRECTION('ref_axis',(1.,0.,0.));
#4181=DIRECTION('center_axis',(0.,0.,-1.));
#4182=DIRECTION('ref_axis',(1.,0.,0.));
#4183=DIRECTION('center_axis',(0.,0.,-1.));
#4184=DIRECTION('ref_axis',(-1.,0.,0.));
#4185=DIRECTION('',(-0.0871557427578718,1.06735001395738E-17,0.996194698090852));
#5121=CARTESIAN_POINT('',(0.,0.,0.));
#5122=CARTESIAN_POINT('Origin',(-1.41899999999985,1.41899999999965,3.1));
#5123=CARTESIAN_POINT('',(-1.41899999999985,0.472999999999654,3.01252522110193));
#5124=CARTESIAN_POINT('',(-0.472999999999848,1.41899999999969,3.01252522110194));
#5125=CARTESIAN_POINT('Ctrl Pts',(-1.41899999999985,0.472999999999654,3.01252522110193));
#5126=CARTESIAN_POINT('Ctrl Pts',(-1.418237843063,0.472999999999654,3.01261008153857));
#5127=CARTESIAN_POINT('Ctrl Pts',(-1.41747599318127,0.473000921064105,3.01269480438576));
#5128=CARTESIAN_POINT('Ctrl Pts',(-1.29873656917598,0.473287797471327,3.02588334070707));
#5129=CARTESIAN_POINT('Ctrl Pts',(-1.17260477262757,0.497030428020145,3.03726209636997));
#5130=CARTESIAN_POINT('Ctrl Pts',(-0.940241249793281,0.593452559529333,
3.05235989856665));
#5131=CARTESIAN_POINT('Ctrl Pts',(-0.834013199901804,0.666140770092746,
3.05607990145755));
#5132=CARTESIAN_POINT('Ctrl Pts',(-0.75007698499736,0.750076984997194,3.05607990145756));
#5133=CARTESIAN_POINT('Ctrl Pts',(-0.666140770092915,0.834013199901643,
3.05607990145756));
#5134=CARTESIAN_POINT('Ctrl Pts',(-0.593452559529506,0.940241249793123,
3.05235989856665));
#5135=CARTESIAN_POINT('Ctrl Pts',(-0.497030428020328,1.17260477262741,3.03726209636997));
#5136=CARTESIAN_POINT('Ctrl Pts',(-0.473287797471517,1.29873656917583,3.02588334070708));
#5137=CARTESIAN_POINT('Ctrl Pts',(-0.4730009210643,1.41747599318095,3.01269480438579));
#5138=CARTESIAN_POINT('Ctrl Pts',(-0.472999999999848,1.41823784306269,3.0126100815386));
#5139=CARTESIAN_POINT('Ctrl Pts',(-0.472999999999848,1.41899999999969,3.01252522110194));
#5140=CARTESIAN_POINT('',(-1.41899999999985,0.472999999999654,1.22765307701778));
#5141=CARTESIAN_POINT('',(-1.41899999999985,0.472999999999654,3.1));
#5142=CARTESIAN_POINT('',(-0.866098738193358,0.651395808574938,0.27));
#5143=CARTESIAN_POINT('Origin',(-1.41899999999985,1.41899999999965,1.22765307701778));
#5144=CARTESIAN_POINT('',(-0.651395808574991,0.86609873819336,0.27));
#5145=CARTESIAN_POINT('Origin',(-1.41899999999985,1.41899999999965,0.27));
#5146=CARTESIAN_POINT('',(-0.472999999999848,1.41899999999969,1.22765307701751));
#5147=CARTESIAN_POINT('Origin',(-1.41899999999985,1.41899999999965,1.22765307701745));
#5148=CARTESIAN_POINT('',(-0.472999999999848,1.41899999999969,3.1));
#5149=CARTESIAN_POINT('Origin',(-0.472999999999807,0.472999999999754,3.1));
#5150=CARTESIAN_POINT('',(-0.472999999999889,2.36767196216383,2.87080111520185));
#5151=CARTESIAN_POINT('Origin',(-0.472999999999787,-2.0353210154902E-14,
-9.73193776093083));
#5152=CARTESIAN_POINT('',(-0.472999999999884,2.24662499999997,2.66114162663218));
#5153=CARTESIAN_POINT('Origin',(-0.472999999999895,2.5,3.1));
#5154=CARTESIAN_POINT('',(0.472999999999787,2.36767196216383,2.87080111520185));
#5155=CARTESIAN_POINT('Origin',(1.16338464595253E-14,-3.68139204037345,
-7.60648507542867));
#5156=CARTESIAN_POINT('',(0.651395808575038,0.866098738193364,0.27));
#5157=CARTESIAN_POINT('',(-0.236499999999946,0.866098738193362,0.27));
#5158=CARTESIAN_POINT('',(0.472999999999754,1.41899999999989,1.22765307701784));
#5159=CARTESIAN_POINT('Origin',(1.41899999999975,1.41899999999985,1.22765307701778));
#5160=CARTESIAN_POINT('',(0.472999999999791,2.5,3.09999999999999));
#5161=CARTESIAN_POINT('Origin',(0.472999999999791,2.5,3.1));
#5162=CARTESIAN_POINT('',(0.472999999999754,1.41899999999989,3.01252522110192));
#5163=CARTESIAN_POINT('Origin',(0.472999999999705,-1.6370004348928E-14,
-9.73193776093083));
#5164=CARTESIAN_POINT('',(0.472999999999754,1.41899999999989,3.1));
#5165=CARTESIAN_POINT('Origin',(1.41899999999975,1.41899999999985,3.1));
#5166=CARTESIAN_POINT('',(1.41899999999979,0.472999999999854,3.01252522110193));
#5167=CARTESIAN_POINT('Ctrl Pts',(0.472999999999754,1.41899999999989,3.01252522110192));
#5168=CARTESIAN_POINT('Ctrl Pts',(0.472999999999754,1.41823784306304,3.01261008153856));
#5169=CARTESIAN_POINT('Ctrl Pts',(0.473000921064206,1.4174759931813,3.01269480438575));
#5170=CARTESIAN_POINT('Ctrl Pts',(0.473287797471426,1.29873656917601,3.02588334070706));
#5171=CARTESIAN_POINT('Ctrl Pts',(0.49703042802024,1.17260477262759,3.03726209636996));
#5172=CARTESIAN_POINT('Ctrl Pts',(0.593452559529424,0.940241249793303,3.05235989856665));
#5173=CARTESIAN_POINT('Ctrl Pts',(0.666140770092836,0.834013199901824,3.05607990145755));
#5174=CARTESIAN_POINT('Ctrl Pts',(0.750076984997282,0.750076984997378,3.05607990145755));
#5175=CARTESIAN_POINT('Ctrl Pts',(0.834013199901729,0.666140770092932,3.05607990145755));
#5176=CARTESIAN_POINT('Ctrl Pts',(0.940241249793208,0.593452559529521,3.05235989856665));
#5177=CARTESIAN_POINT('Ctrl Pts',(1.1726047726275,0.497030428020338,3.03726209636996));
#5178=CARTESIAN_POINT('Ctrl Pts',(1.29873656917591,0.473287797471525,3.02588334070707));
#5179=CARTESIAN_POINT('Ctrl Pts',(1.41747599318104,0.473000921064306,3.01269480438578));
#5180=CARTESIAN_POINT('Ctrl Pts',(1.41823784306278,0.472999999999854,3.01261008153858));
#5181=CARTESIAN_POINT('Ctrl Pts',(1.41899999999979,0.472999999999854,3.01252522110193));
#5182=CARTESIAN_POINT('',(0.866098738193361,0.651395808575069,0.27));
#5183=CARTESIAN_POINT('Origin',(1.41899999999975,1.41899999999985,0.27));
#5184=CARTESIAN_POINT('',(1.41899999999979,0.472999999999853,1.22765307701768));
#5185=CARTESIAN_POINT('Origin',(1.41899999999975,1.41899999999985,1.22765307701762));
#5186=CARTESIAN_POINT('',(1.41899999999979,0.472999999999854,3.1));
#5187=CARTESIAN_POINT('Origin',(0.472999999999817,0.472999999999815,3.1));
#5188=CARTESIAN_POINT('',(2.36767196216383,0.472999999999892,2.87080111520185));
#5189=CARTESIAN_POINT('Origin',(-1.83061508724184E-14,0.472999999999796,
-9.73193776093083));
#5190=CARTESIAN_POINT('',(2.24662499999998,0.472999999999887,2.6611416266322));
#5191=CARTESIAN_POINT('Origin',(2.5,0.472999999999897,3.1));
#5192=CARTESIAN_POINT('',(2.36767196216383,-0.472999999999786,2.87080111520185));
#5193=CARTESIAN_POINT('Origin',(-3.68139204037345,0.,-7.60648507542867));
#5194=CARTESIAN_POINT('',(0.866098738193361,-0.65139580857508,0.270000000000001));
#5195=CARTESIAN_POINT('',(0.86609873819336,0.236499999999951,0.27));
#5196=CARTESIAN_POINT('',(1.41899999999987,-0.472999999999785,1.22765307701781));
#5197=CARTESIAN_POINT('Origin',(1.41899999999987,-1.41899999999979,1.22765307701781));
#5198=CARTESIAN_POINT('',(2.5,-0.472999999999786,3.1));
#5199=CARTESIAN_POINT('Origin',(2.5,-0.472999999999786,3.1));
#5200=CARTESIAN_POINT('',(1.41899999999987,-0.472999999999785,3.01252522110192));
#5201=CARTESIAN_POINT('Origin',(6.05980759185948E-16,-0.472999999999784,
-9.73193776093083));
#5202=CARTESIAN_POINT('',(1.41899999999987,-0.472999999999785,3.1));
#5203=CARTESIAN_POINT('Origin',(-1.41899999999978,-1.41899999999983,3.1));
#5204=CARTESIAN_POINT('',(-0.472999999999784,-1.41899999999984,3.01252522110192));
#5205=CARTESIAN_POINT('',(-1.41899999999983,-0.472999999999835,3.01252522110192));
#5206=CARTESIAN_POINT('Ctrl Pts',(-0.472999999999784,-1.41899999999984,
3.01252522110192));
#5207=CARTESIAN_POINT('Ctrl Pts',(-0.472999999999784,-1.41823784306299,
3.01261008153856));
#5208=CARTESIAN_POINT('Ctrl Pts',(-0.473000921064235,-1.41747599318126,
3.01269480438576));
#5209=CARTESIAN_POINT('Ctrl Pts',(-0.473287797471458,-1.29873656917597,
3.02588334070707));
#5210=CARTESIAN_POINT('Ctrl Pts',(-0.497030428020275,-1.17260477262755,
3.03726209636996));
#5211=CARTESIAN_POINT('Ctrl Pts',(-0.593452559529464,-0.940241249793266,
3.05235989856664));
#5212=CARTESIAN_POINT('Ctrl Pts',(-0.666140770092878,-0.834013199901788,
3.05607990145755));
#5213=CARTESIAN_POINT('Ctrl Pts',(-0.750076984997327,-0.750076984997344,
3.05607990145755));
#5214=CARTESIAN_POINT('Ctrl Pts',(-0.834013199901775,-0.6661407700929,3.05607990145755));
#5215=CARTESIAN_POINT('Ctrl Pts',(-0.940241249793256,-0.593452559529491,
3.05235989856665));
#5216=CARTESIAN_POINT('Ctrl Pts',(-1.17260477262755,-0.497030428020314,
3.03726209636996));
#5217=CARTESIAN_POINT('Ctrl Pts',(-1.29873656917596,-0.473287797471503,
3.02588334070706));
#5218=CARTESIAN_POINT('Ctrl Pts',(-1.41747599318109,-0.473000921064287,
3.01269480438577));
#5219=CARTESIAN_POINT('Ctrl Pts',(-1.41823784306282,-0.472999999999835,
3.01261008153858));
#5220=CARTESIAN_POINT('Ctrl Pts',(-1.41899999999983,-0.472999999999835,
3.01252522110192));
#5221=CARTESIAN_POINT('',(-0.472999999999784,-1.41899999999984,1.22765307701777));
#5222=CARTESIAN_POINT('',(-0.472999999999784,-1.41899999999984,3.1));
#5223=CARTESIAN_POINT('',(-0.651395808575061,-0.866098738193354,0.27));
#5224=CARTESIAN_POINT('Origin',(-1.41899999999978,-1.41899999999983,1.22765307701777));
#5225=CARTESIAN_POINT('',(-0.866098738193358,-0.651395808575073,0.27));
#5226=CARTESIAN_POINT('Origin',(-1.41899999999978,-1.41899999999983,0.27));
#5227=CARTESIAN_POINT('',(-1.41899999999983,-0.472999999999835,1.22765307701776));
#5228=CARTESIAN_POINT('Origin',(-1.41899999999978,-1.41899999999983,1.22765307701767));
#5229=CARTESIAN_POINT('',(-1.41899999999983,-0.472999999999835,3.1));
#5230=CARTESIAN_POINT('Origin',(-0.472999999999781,-0.472999999999784,3.1));
#5231=CARTESIAN_POINT('',(-2.36767196216382,-0.472999999999886,2.87080111520185));
#5232=CARTESIAN_POINT('Origin',(2.61729806275939E-14,-0.472999999999759,
-9.73193776093083));
#5233=CARTESIAN_POINT('',(-2.24662499999997,-0.472999999999879,2.66114162663219));
#5234=CARTESIAN_POINT('Origin',(1.41899999999987,-1.41899999999979,3.1));
#5235=CARTESIAN_POINT('',(0.472999999999865,-1.41899999999981,3.01252522110192));
#5236=CARTESIAN_POINT('Ctrl Pts',(1.41899999999987,-0.472999999999785,3.01252522110192));
#5237=CARTESIAN_POINT('Ctrl Pts',(1.41823784306302,-0.472999999999785,3.01261008153856));
#5238=CARTESIAN_POINT('Ctrl Pts',(1.41747599318129,-0.473000921064237,3.01269480438575));
#5239=CARTESIAN_POINT('Ctrl Pts',(1.29873656917601,-0.473287797471458,3.02588334070706));
#5240=CARTESIAN_POINT('Ctrl Pts',(1.17260477262759,-0.497030428020274,3.03726209636996));
#5241=CARTESIAN_POINT('Ctrl Pts',(0.940241249793305,-0.59345255952946,3.05235989856664));
#5242=CARTESIAN_POINT('Ctrl Pts',(0.834013199901827,-0.666140770092873,
3.05607990145755));
#5243=CARTESIAN_POINT('Ctrl Pts',(0.750076984997382,-0.75007698499732,3.05607990145755));
#5244=CARTESIAN_POINT('Ctrl Pts',(0.666140770092937,-0.834013199901768,
3.05607990145755));
#5245=CARTESIAN_POINT('Ctrl Pts',(0.593452559529527,-0.940241249793248,
3.05235989856665));
#5246=CARTESIAN_POINT('Ctrl Pts',(0.497030428020347,-1.17260477262754,3.03726209636996));
#5247=CARTESIAN_POINT('Ctrl Pts',(0.473287797471535,-1.29873656917595,3.02588334070706));
#5248=CARTESIAN_POINT('Ctrl Pts',(0.473000921064317,-1.41747599318107,3.01269480438577));
#5249=CARTESIAN_POINT('Ctrl Pts',(0.472999999999865,-1.4182378430628,3.01261008153858));
#5250=CARTESIAN_POINT('Ctrl Pts',(0.472999999999865,-1.41899999999981,3.01252522110192));
#5251=CARTESIAN_POINT('',(0.651395808575106,-0.866098738193356,0.27));
#5252=CARTESIAN_POINT('Origin',(1.41899999999987,-1.41899999999979,0.27));
#5253=CARTESIAN_POINT('',(0.472999999999865,-1.41899999999981,1.22765307701772));
#5254=CARTESIAN_POINT('Origin',(1.41899999999987,-1.41899999999979,1.22765307701768));
#5255=CARTESIAN_POINT('',(0.472999999999865,-1.41899999999981,3.1));
#5256=CARTESIAN_POINT('Origin',(0.472999999999839,-0.472999999999785,3.1));
#5257=CARTESIAN_POINT('',(0.472999999999892,-2.36767196216382,2.87080111520185));
#5258=CARTESIAN_POINT('Origin',(0.472999999999825,1.32935445800918E-14,
-9.73193776093083));
#5259=CARTESIAN_POINT('',(0.472999999999889,-2.24662499999997,2.66114162663219));
#5260=CARTESIAN_POINT('Origin',(-2.5,0.472999999999654,3.1));
#5261=CARTESIAN_POINT('',(-2.36767196216383,0.472999999999654,2.87080111520186));
#5262=CARTESIAN_POINT('Origin',(8.32667268468867E-16,0.472999999999654,
-9.73193776093083));
#5263=CARTESIAN_POINT('',(-2.5,0.472999999999654,3.1));
#5264=CARTESIAN_POINT('Origin',(-2.5,-0.472999999999893,3.1));
#5265=CARTESIAN_POINT('',(-2.37229341204248,-2.90522153369617E-16,2.87880570119631));
#5266=CARTESIAN_POINT('Origin',(3.68139204037345,0.,-7.60648507542867));
#5267=CARTESIAN_POINT('',(-0.866098738193358,-0.236499999999945,0.27));
#5268=CARTESIAN_POINT('Origin',(3.68139204037345,0.,-7.60648507542867));
#5269=CARTESIAN_POINT('Origin',(-0.472999999999788,-2.5,3.1));
#5270=CARTESIAN_POINT('',(-0.472999999999788,-2.36767196216382,2.87080111520185));
#5271=CARTESIAN_POINT('Origin',(-0.472999999999779,1.82968396778355E-15,
-9.73193776093083));
#5272=CARTESIAN_POINT('',(-0.472999999999788,-2.5,3.1));
#5273=CARTESIAN_POINT('Origin',(0.472999999999896,-2.5,3.1));
#5274=CARTESIAN_POINT('Origin',(6.23325686399709E-15,3.68139204037346,-7.60648507542867));
#5275=CARTESIAN_POINT('',(0.236499999999949,-0.866098738193356,0.27));
#5276=CARTESIAN_POINT('Origin',(1.11022302462516E-15,3.88578058618805E-15,
0.27));
#5277=CARTESIAN_POINT('Origin',(0.,0.,-0.2));
#5278=CARTESIAN_POINT('',(2.37846096908266,-2.91277461268399E-16,-3.46944695195361E-17));
#5279=CARTESIAN_POINT('Origin',(0.,0.,-3.46944695195361E-17));
#5280=CARTESIAN_POINT('',(2.17846096908266,-2.66784525285452E-16,-0.2));
#5281=CARTESIAN_POINT('Origin',(2.37846096908266,-2.91277461268399E-16,
-0.2));
#5282=CARTESIAN_POINT('Origin',(0.,0.,-0.2));
#5283=CARTESIAN_POINT('Origin',(-2.17846096908266,0.,-1.88141750998334E-17));
#5284=CARTESIAN_POINT('',(5.15,-6.30693101560887E-16,-2.77555756156289E-16));
#5285=CARTESIAN_POINT('Origin',(0.,0.,0.));
#5286=CARTESIAN_POINT('Origin',(0.,0.,-0.149999999999999));
#5287=CARTESIAN_POINT('',(2.17846096908266,-2.66784525285452E-16,-0.299999999999998));
#5288=CARTESIAN_POINT('Origin',(0.,0.,-0.299999999999998));
#5289=CARTESIAN_POINT('',(2.17846096908266,-2.66784525285452E-16,-0.149999999999999));
#5290=CARTESIAN_POINT('Origin',(0.,0.,-0.899999999999999));
#5291=CARTESIAN_POINT('',(2.4505,-3.00099698131059E-16,-1.31526348502534));
#5292=CARTESIAN_POINT('Origin',(0.,0.,-1.31526348502534));
#5293=CARTESIAN_POINT('',(2.33923048454133,-2.86473112536145E-16,-0.899999999999999));
#5294=CARTESIAN_POINT('Origin',(0.,0.,-7.75));
#5295=CARTESIAN_POINT('',(2.4505,3.00099698131059E-16,-14.));
#5296=CARTESIAN_POINT('Origin',(0.,0.,-14.));
#5297=CARTESIAN_POINT('',(2.4505,-3.00099698131059E-16,-7.75));
#5298=CARTESIAN_POINT('Origin',(0.,0.,-14.));
#5299=CARTESIAN_POINT('Origin',(8.32667268468867E-16,0.,-9.73193776093083));
#5300=CARTESIAN_POINT('',(-4.96627380657387,0.,2.1));
#5301=CARTESIAN_POINT('Origin',(8.32667268468867E-16,0.,-9.73193776093083));
#5302=CARTESIAN_POINT('',(4.96627380657386,-6.08193132091002E-16,2.1));
#5303=CARTESIAN_POINT('Origin',(0.,0.,2.1));
#5304=CARTESIAN_POINT('Origin',(0.,0.,2.1));
#5305=CARTESIAN_POINT('Origin',(0.,0.,1.05));
#5306=CARTESIAN_POINT('',(5.05813690328693,-6.19443116825945E-16,1.05));
#7026=UNCERTAINTY_MEASURE_WITH_UNIT(LENGTH_MEASURE(0.01),#7048,
'DISTANCE_ACCURACY_VALUE',
'Maximum model space distance between geometric entities at asserted c
onnectivities');
#7035=UNCERTAINTY_MEASURE_WITH_UNIT(LENGTH_MEASURE(0.01),#7048,
'DISTANCE_ACCURACY_VALUE',
'Maximum model space distance between geometric entities at asserted c
onnectivities');
#7038=(
GEOMETRIC_REPRESENTATION_CONTEXT(3)
GLOBAL_UNCERTAINTY_ASSIGNED_CONTEXT((#7026))
GLOBAL_UNIT_ASSIGNED_CONTEXT((#7048,#7050,#7051))
REPRESENTATION_CONTEXT('','3D')
);
#7047=(
GEOMETRIC_REPRESENTATION_CONTEXT(3)
GLOBAL_UNCERTAINTY_ASSIGNED_CONTEXT((#7035))
GLOBAL_UNIT_ASSIGNED_CONTEXT((#7048,#7050,#7051))
REPRESENTATION_CONTEXT('','3D')
);
#7048=(
LENGTH_UNIT()
NAMED_UNIT(*)
SI_UNIT(.MILLI.,.METRE.)
);
#7050=(
NAMED_UNIT(*)
PLANE_ANGLE_UNIT()
SI_UNIT($,.RADIAN.)
);
#7051=(
NAMED_UNIT(*)
SI_UNIT($,.STERADIAN.)
SOLID_ANGLE_UNIT()
);
#7054=SHAPE_DEFINITION_REPRESENTATION(#7065,#7086);
#7065=PRODUCT_DEFINITION_SHAPE('',$,#7098);
#7086=SHAPE_REPRESENTATION('',(#3580),#7038);
#7095=PRODUCT_DEFINITION_CONTEXT('part definition',#7130,'design');
#7098=PRODUCT_DEFINITION('BHS JIS B 1111 - M5x14 Steel 4.6 Plain_1',
'M5x14 Steel 4.6 Plain v1 (1)',#7109,#7095);
#7109=PRODUCT_DEFINITION_FORMATION('',$,#7134);
#7130=APPLICATION_CONTEXT(
'Core Data for Automotive Mechanical Design Process');
#7131=PRODUCT_CONTEXT('part definition',#7130,'mechanical');
#7134=PRODUCT('BHS JIS B 1111 - M5x14 Steel 4.6 Plain_1',
'M5x14 Steel 4.6 Plain v1 (1)','Binding Head Screw JIS B 1111 - M5x14',
(#7131));
#7206=COLOUR_RGB('Off White',0.89,0.88,0.83);
#7207=FILL_AREA_STYLE_COLOUR('',#7206);
#7208=FILL_AREA_STYLE('',(#7207));
#7209=SURFACE_STYLE_FILL_AREA(#7208);
#7210=SURFACE_SIDE_STYLE('',(#7209));
#7211=SURFACE_STYLE_USAGE(.BOTH.,#7210);
#7212=PRESENTATION_STYLE_ASSIGNMENT((#7211));
ENDSEC;
END-ISO-10303-21;
